ISO-10303-21;
HEADER;
/* Generated by software containing ST-Developer
 * from STEP Tools, Inc. (www.steptools.com) 
 */

FILE_DESCRIPTION(
/* description */ ('Worm-less right-angle friction wheel drive'),
/* implementation_level */ '2;1');

FILE_NAME(
/* name */ 'Bearing cap (2).step',
/* time_stamp */ '2026-10-28T03:22:36-07:00',
/* author */ (''),
/* organization */ (''),
/* preprocessor_version */ 'ST-DEVELOPER v20.2',
/* originating_system */ 'Autodesk Translation Framework v15.17.0.0',
/* authorisation */ '');

FILE_SCHEMA (('AUTOMOTIVE_DESIGN { 1 0 10303 214 3 1 1 }'));
ENDSEC;

DATA;
#10=MECHANICAL_DESIGN_GEOMETRIC_PRESENTATION_REPRESENTATION('',(#619),#17046);
#525=SHAPE_REPRESENTATION_RELATIONSHIP('SRR','None',#17268,#572);
#572=ADVANCED_BREP_SHAPE_REPRESENTATION('',(#673),#17004);
#619=STYLED_ITEM('',(#17591),#673);
#673=MANIFOLD_SOLID_BREP('Body1',#8174);
#801=FACE_BOUND('',#1874,.T.);
#802=FACE_BOUND('',#1878,.T.);
#803=FACE_BOUND('',#1879,.T.);
#804=FACE_BOUND('',#1880,.T.);
#805=FACE_BOUND('',#1881,.T.);
#806=FACE_BOUND('',#1882,.T.);
#807=FACE_BOUND('',#1884,.T.);
#808=FACE_BOUND('',#1885,.T.);
#809=FACE_BOUND('',#1886,.T.);
#810=FACE_BOUND('',#1887,.T.);
#811=FACE_BOUND('',#1888,.T.);
#1010=PLANE('',#8976);
#1011=PLANE('',#8983);
#1012=PLANE('',#8984);
#1316=FACE_OUTER_BOUND('',#1868,.T.);
#1317=FACE_OUTER_BOUND('',#1869,.T.);
#1318=FACE_OUTER_BOUND('',#1870,.T.);
#1319=FACE_OUTER_BOUND('',#1871,.T.);
#1320=FACE_OUTER_BOUND('',#1872,.T.);
#1321=FACE_OUTER_BOUND('',#1873,.T.);
#1322=FACE_OUTER_BOUND('',#1875,.T.);
#1323=FACE_OUTER_BOUND('',#1876,.T.);
#1324=FACE_OUTER_BOUND('',#1877,.T.);
#1325=FACE_OUTER_BOUND('',#1883,.T.);
#1868=EDGE_LOOP('',(#6074,#6075,#6076,#6077));
#1869=EDGE_LOOP('',(#6078,#6079,#6080,#6081));
#1870=EDGE_LOOP('',(#6082,#6083,#6084,#6085));
#1871=EDGE_LOOP('',(#6086,#6087,#6088,#6089));
#1872=EDGE_LOOP('',(#6090,#6091,#6092,#6093));
#1873=EDGE_LOOP('',(#6094));
#1874=EDGE_LOOP('',(#6095));
#1875=EDGE_LOOP('',(#6096,#6097,#6098,#6099));
#1876=EDGE_LOOP('',(#6100,#6101,#6102,#6103));
#1877=EDGE_LOOP('',(#6104));
#1878=EDGE_LOOP('',(#6105));
#1879=EDGE_LOOP('',(#6106));
#1880=EDGE_LOOP('',(#6107));
#1881=EDGE_LOOP('',(#6108));
#1882=EDGE_LOOP('',(#6109));
#1883=EDGE_LOOP('',(#6110));
#1884=EDGE_LOOP('',(#6111));
#1885=EDGE_LOOP('',(#6112));
#1886=EDGE_LOOP('',(#6113));
#1887=EDGE_LOOP('',(#6114));
#1888=EDGE_LOOP('',(#6115));
#2547=LINE('',#12948,#3087);
#2548=LINE('',#12954,#3088);
#2549=LINE('',#12960,#3089);
#2550=LINE('',#12966,#3090);
#2551=LINE('',#12972,#3091);
#2552=LINE('',#12979,#3092);
#2553=LINE('',#12985,#3093);
#3087=VECTOR('',#10385,0.225);
#3088=VECTOR('',#10392,0.225);
#3089=VECTOR('',#10399,0.225);
#3090=VECTOR('',#10406,0.225);
#3091=VECTOR('',#10413,1.59);
#3092=VECTOR('',#10422,1.2);
#3093=VECTOR('',#10429,2.4);
#3557=CIRCLE('',#8962,0.225);
#3558=CIRCLE('',#8963,0.225);
#3559=CIRCLE('',#8965,0.225);
#3560=CIRCLE('',#8966,0.225);
#3561=CIRCLE('',#8968,0.225);
#3562=CIRCLE('',#8969,0.225);
#3563=CIRCLE('',#8971,0.225);
#3564=CIRCLE('',#8972,0.225);
#3565=CIRCLE('',#8974,1.59);
#3566=CIRCLE('',#8975,1.59);
#3567=CIRCLE('',#8977,1.2);
#3568=CIRCLE('',#8979,1.2);
#3569=CIRCLE('',#8981,2.4);
#3570=CIRCLE('',#8982,2.4);
#4049=VERTEX_POINT('',#12945);
#4050=VERTEX_POINT('',#12947);
#4051=VERTEX_POINT('',#12951);
#4052=VERTEX_POINT('',#12953);
#4053=VERTEX_POINT('',#12957);
#4054=VERTEX_POINT('',#12959);
#4055=VERTEX_POINT('',#12963);
#4056=VERTEX_POINT('',#12965);
#4057=VERTEX_POINT('',#12969);
#4058=VERTEX_POINT('',#12971);
#4059=VERTEX_POINT('',#12975);
#4060=VERTEX_POINT('',#12978);
#4061=VERTEX_POINT('',#12982);
#4062=VERTEX_POINT('',#12984);
#4806=EDGE_CURVE('',#4049,#4049,#3557,.T.);
#4807=EDGE_CURVE('',#4049,#4050,#2547,.T.);
#4808=EDGE_CURVE('',#4050,#4050,#3558,.T.);
#4809=EDGE_CURVE('',#4051,#4051,#3559,.T.);
#4810=EDGE_CURVE('',#4051,#4052,#2548,.T.);
#4811=EDGE_CURVE('',#4052,#4052,#3560,.T.);
#4812=EDGE_CURVE('',#4053,#4053,#3561,.T.);
#4813=EDGE_CURVE('',#4053,#4054,#2549,.T.);
#4814=EDGE_CURVE('',#4054,#4054,#3562,.T.);
#4815=EDGE_CURVE('',#4055,#4055,#3563,.T.);
#4816=EDGE_CURVE('',#4055,#4056,#2550,.T.);
#4817=EDGE_CURVE('',#4056,#4056,#3564,.T.);
#4818=EDGE_CURVE('',#4057,#4057,#3565,.T.);
#4819=EDGE_CURVE('',#4057,#4058,#2551,.T.);
#4820=EDGE_CURVE('',#4058,#4058,#3566,.T.);
#4821=EDGE_CURVE('',#4059,#4059,#3567,.T.);
#4822=EDGE_CURVE('',#4059,#4060,#2552,.T.);
#4823=EDGE_CURVE('',#4060,#4060,#3568,.T.);
#4824=EDGE_CURVE('',#4061,#4061,#3569,.T.);
#4825=EDGE_CURVE('',#4061,#4062,#2553,.T.);
#4826=EDGE_CURVE('',#4062,#4062,#3570,.T.);
#6074=ORIENTED_EDGE('',*,*,#4806,.F.);
#6075=ORIENTED_EDGE('',*,*,#4807,.T.);
#6076=ORIENTED_EDGE('',*,*,#4808,.F.);
#6077=ORIENTED_EDGE('',*,*,#4807,.F.);
#6078=ORIENTED_EDGE('',*,*,#4809,.F.);
#6079=ORIENTED_EDGE('',*,*,#4810,.T.);
#6080=ORIENTED_EDGE('',*,*,#4811,.F.);
#6081=ORIENTED_EDGE('',*,*,#4810,.F.);
#6082=ORIENTED_EDGE('',*,*,#4812,.F.);
#6083=ORIENTED_EDGE('',*,*,#4813,.T.);
#6084=ORIENTED_EDGE('',*,*,#4814,.F.);
#6085=ORIENTED_EDGE('',*,*,#4813,.F.);
#6086=ORIENTED_EDGE('',*,*,#4815,.F.);
#6087=ORIENTED_EDGE('',*,*,#4816,.T.);
#6088=ORIENTED_EDGE('',*,*,#4817,.F.);
#6089=ORIENTED_EDGE('',*,*,#4816,.F.);
#6090=ORIENTED_EDGE('',*,*,#4818,.F.);
#6091=ORIENTED_EDGE('',*,*,#4819,.T.);
#6092=ORIENTED_EDGE('',*,*,#4820,.F.);
#6093=ORIENTED_EDGE('',*,*,#4819,.F.);
#6094=ORIENTED_EDGE('',*,*,#4818,.T.);
#6095=ORIENTED_EDGE('',*,*,#4821,.T.);
#6096=ORIENTED_EDGE('',*,*,#4821,.F.);
#6097=ORIENTED_EDGE('',*,*,#4822,.T.);
#6098=ORIENTED_EDGE('',*,*,#4823,.T.);
#6099=ORIENTED_EDGE('',*,*,#4822,.F.);
#6100=ORIENTED_EDGE('',*,*,#4824,.F.);
#6101=ORIENTED_EDGE('',*,*,#4825,.T.);
#6102=ORIENTED_EDGE('',*,*,#4826,.T.);
#6103=ORIENTED_EDGE('',*,*,#4825,.F.);
#6104=ORIENTED_EDGE('',*,*,#4824,.T.);
#6105=ORIENTED_EDGE('',*,*,#4820,.T.);
#6106=ORIENTED_EDGE('',*,*,#4817,.T.);
#6107=ORIENTED_EDGE('',*,*,#4814,.T.);
#6108=ORIENTED_EDGE('',*,*,#4811,.T.);
#6109=ORIENTED_EDGE('',*,*,#4808,.T.);
#6110=ORIENTED_EDGE('',*,*,#4826,.F.);
#6111=ORIENTED_EDGE('',*,*,#4823,.F.);
#6112=ORIENTED_EDGE('',*,*,#4815,.T.);
#6113=ORIENTED_EDGE('',*,*,#4812,.T.);
#6114=ORIENTED_EDGE('',*,*,#4809,.T.);
#6115=ORIENTED_EDGE('',*,*,#4806,.T.);
#7580=CYLINDRICAL_SURFACE('',#8961,0.225);
#7581=CYLINDRICAL_SURFACE('',#8964,0.225);
#7582=CYLINDRICAL_SURFACE('',#8967,0.225);
#7583=CYLINDRICAL_SURFACE('',#8970,0.225);
#7584=CYLINDRICAL_SURFACE('',#8973,1.59);
#7585=CYLINDRICAL_SURFACE('',#8978,1.2);
#7586=CYLINDRICAL_SURFACE('',#8980,2.4);
#7808=ADVANCED_FACE('',(#1316),#7580,.F.);
#7809=ADVANCED_FACE('',(#1317),#7581,.F.);
#7810=ADVANCED_FACE('',(#1318),#7582,.F.);
#7811=ADVANCED_FACE('',(#1319),#7583,.F.);
#7812=ADVANCED_FACE('',(#1320),#7584,.T.);
#7813=ADVANCED_FACE('',(#1321,#801),#1010,.T.);
#7814=ADVANCED_FACE('',(#1322),#7585,.F.);
#7815=ADVANCED_FACE('',(#1323),#7586,.T.);
#7816=ADVANCED_FACE('',(#1324,#802,#803,#804,#805,#806),#1011,.T.);
#7817=ADVANCED_FACE('',(#1325,#807,#808,#809,#810,#811),#1012,.F.);
#8174=CLOSED_SHELL('',(#7808,#7809,#7810,#7811,#7812,#7813,#7814,#7815,
#7816,#7817));
#8960=AXIS2_PLACEMENT_3D('',#12943,#10379,#10380);
#8961=AXIS2_PLACEMENT_3D('',#12944,#10381,#10382);
#8962=AXIS2_PLACEMENT_3D('',#12946,#10383,#10384);
#8963=AXIS2_PLACEMENT_3D('',#12949,#10386,#10387);
#8964=AXIS2_PLACEMENT_3D('',#12950,#10388,#10389);
#8965=AXIS2_PLACEMENT_3D('',#12952,#10390,#10391);
#8966=AXIS2_PLACEMENT_3D('',#12955,#10393,#10394);
#8967=AXIS2_PLACEMENT_3D('',#12956,#10395,#10396);
#8968=AXIS2_PLACEMENT_3D('',#12958,#10397,#10398);
#8969=AXIS2_PLACEMENT_3D('',#12961,#10400,#10401);
#8970=AXIS2_PLACEMENT_3D('',#12962,#10402,#10403);
#8971=AXIS2_PLACEMENT_3D('',#12964,#10404,#10405);
#8972=AXIS2_PLACEMENT_3D('',#12967,#10407,#10408);
#8973=AXIS2_PLACEMENT_3D('',#12968,#10409,#10410);
#8974=AXIS2_PLACEMENT_3D('',#12970,#10411,#10412);
#8975=AXIS2_PLACEMENT_3D('',#12973,#10414,#10415);
#8976=AXIS2_PLACEMENT_3D('',#12974,#10416,#10417);
#8977=AXIS2_PLACEMENT_3D('',#12976,#10418,#10419);
#8978=AXIS2_PLACEMENT_3D('',#12977,#10420,#10421);
#8979=AXIS2_PLACEMENT_3D('',#12980,#10423,#10424);
#8980=AXIS2_PLACEMENT_3D('',#12981,#10425,#10426);
#8981=AXIS2_PLACEMENT_3D('',#12983,#10427,#10428);
#8982=AXIS2_PLACEMENT_3D('',#12986,#10430,#10431);
#8983=AXIS2_PLACEMENT_3D('',#12987,#10432,#10433);
#8984=AXIS2_PLACEMENT_3D('',#12988,#10434,#10435);
#10379=DIRECTION('axis',(0.,0.,1.));
#10380=DIRECTION('refdir',(1.,0.,0.));
#10381=DIRECTION('center_axis',(0.,1.,0.));
#10382=DIRECTION('ref_axis',(1.,0.,0.));
#10383=DIRECTION('center_axis',(0.,1.,0.));
#10384=DIRECTION('ref_axis',(1.,0.,0.));
#10385=DIRECTION('',(0.,1.,0.));
#10386=DIRECTION('center_axis',(0.,-1.,0.));
#10387=DIRECTION('ref_axis',(1.,0.,0.));
#10388=DIRECTION('center_axis',(0.,1.,0.));
#10389=DIRECTION('ref_axis',(1.,0.,0.));
#10390=DIRECTION('center_axis',(0.,1.,0.));
#10391=DIRECTION('ref_axis',(1.,0.,0.));
#10392=DIRECTION('',(0.,1.,0.));
#10393=DIRECTION('center_axis',(0.,-1.,0.));
#10394=DIRECTION('ref_axis',(1.,0.,0.));
#10395=DIRECTION('center_axis',(0.,1.,0.));
#10396=DIRECTION('ref_axis',(1.,0.,0.));
#10397=DIRECTION('center_axis',(0.,1.,0.));
#10398=DIRECTION('ref_axis',(1.,0.,0.));
#10399=DIRECTION('',(0.,1.,0.));
#10400=DIRECTION('center_axis',(0.,-1.,0.));
#10401=DIRECTION('ref_axis',(1.,0.,0.));
#10402=DIRECTION('center_axis',(0.,1.,0.));
#10403=DIRECTION('ref_axis',(1.,0.,0.));
#10404=DIRECTION('center_axis',(0.,1.,0.));
#10405=DIRECTION('ref_axis',(1.,0.,0.));
#10406=DIRECTION('',(0.,1.,0.));
#10407=DIRECTION('center_axis',(0.,-1.,0.));
#10408=DIRECTION('ref_axis',(1.,0.,0.));
#10409=DIRECTION('center_axis',(0.,1.,0.));
#10410=DIRECTION('ref_axis',(1.,0.,0.));
#10411=DIRECTION('center_axis',(0.,1.,0.));
#10412=DIRECTION('ref_axis',(1.,0.,0.));
#10413=DIRECTION('',(0.,-1.,0.));
#10414=DIRECTION('center_axis',(0.,-1.,0.));
#10415=DIRECTION('ref_axis',(1.,0.,0.));
#10416=DIRECTION('center_axis',(0.,1.,0.));
#10417=DIRECTION('ref_axis',(1.,0.,0.));
#10418=DIRECTION('center_axis',(0.,-1.,0.));
#10419=DIRECTION('ref_axis',(1.,0.,0.));
#10420=DIRECTION('center_axis',(0.,1.,0.));
#10421=DIRECTION('ref_axis',(1.,0.,0.));
#10422=DIRECTION('',(0.,-1.,0.));
#10423=DIRECTION('center_axis',(0.,-1.,0.));
#10424=DIRECTION('ref_axis',(1.,0.,0.));
#10425=DIRECTION('center_axis',(0.,1.,0.));
#10426=DIRECTION('ref_axis',(1.,0.,0.));
#10427=DIRECTION('center_axis',(0.,1.,0.));
#10428=DIRECTION('ref_axis',(1.,0.,0.));
#10429=DIRECTION('',(0.,-1.,0.));
#10430=DIRECTION('center_axis',(0.,1.,0.));
#10431=DIRECTION('ref_axis',(1.,0.,0.));
#10432=DIRECTION('center_axis',(0.,1.,0.));
#10433=DIRECTION('ref_axis',(1.,0.,0.));
#10434=DIRECTION('center_axis',(0.,1.,0.));
#10435=DIRECTION('ref_axis',(1.,0.,0.));
#12943=CARTESIAN_POINT('',(0.,0.,0.));
#12944=CARTESIAN_POINT('Origin',(-1.48492424049175,-5.1,5.51507575950825));
#12945=CARTESIAN_POINT('',(-1.70992424049175,-5.,5.51507575950825));
#12946=CARTESIAN_POINT('Origin',(-1.48492424049175,-5.,5.51507575950825));
#12947=CARTESIAN_POINT('',(-1.70992424049175,-4.8,5.51507575950825));
#12948=CARTESIAN_POINT('',(-1.70992424049175,-5.1,5.51507575950825));
#12949=CARTESIAN_POINT('Origin',(-1.48492424049175,-4.8,5.51507575950825));
#12950=CARTESIAN_POINT('Origin',(-1.48492424049175,-5.1,8.48492424049175));
#12951=CARTESIAN_POINT('',(-1.70992424049175,-5.,8.48492424049175));
#12952=CARTESIAN_POINT('Origin',(-1.48492424049175,-5.,8.48492424049175));
#12953=CARTESIAN_POINT('',(-1.70992424049175,-4.8,8.48492424049175));
#12954=CARTESIAN_POINT('',(-1.70992424049175,-5.1,8.48492424049175));
#12955=CARTESIAN_POINT('Origin',(-1.48492424049175,-4.8,8.48492424049175));
#12956=CARTESIAN_POINT('Origin',(1.48492424049175,-5.1,8.48492424049175));
#12957=CARTESIAN_POINT('',(1.25992424049175,-5.,8.48492424049175));
#12958=CARTESIAN_POINT('Origin',(1.48492424049175,-5.,8.48492424049175));
#12959=CARTESIAN_POINT('',(1.25992424049175,-4.8,8.48492424049175));
#12960=CARTESIAN_POINT('',(1.25992424049175,-5.1,8.48492424049175));
#12961=CARTESIAN_POINT('Origin',(1.48492424049175,-4.8,8.48492424049175));
#12962=CARTESIAN_POINT('Origin',(1.48492424049175,-5.1,5.51507575950825));
#12963=CARTESIAN_POINT('',(1.25992424049175,-5.,5.51507575950825));
#12964=CARTESIAN_POINT('Origin',(1.48492424049175,-5.,5.51507575950825));
#12965=CARTESIAN_POINT('',(1.25992424049175,-4.8,5.51507575950825));
#12966=CARTESIAN_POINT('',(1.25992424049175,-5.1,5.51507575950825));
#12967=CARTESIAN_POINT('Origin',(1.48492424049175,-4.8,5.51507575950825));
#12968=CARTESIAN_POINT('Origin',(0.,-4.8,7.));
#12969=CARTESIAN_POINT('',(-1.59,-4.5,7.));
#12970=CARTESIAN_POINT('Origin',(0.,-4.5,7.));
#12971=CARTESIAN_POINT('',(-1.59,-4.8,7.));
#12972=CARTESIAN_POINT('',(-1.59,-4.8,7.));
#12973=CARTESIAN_POINT('Origin',(0.,-4.8,7.));
#12974=CARTESIAN_POINT('Origin',(0.,-4.5,7.));
#12975=CARTESIAN_POINT('',(-1.2,-4.5,7.));
#12976=CARTESIAN_POINT('Origin',(0.,-4.5,7.));
#12977=CARTESIAN_POINT('Origin',(0.,-5.,7.));
#12978=CARTESIAN_POINT('',(-1.2,-5.,7.));
#12979=CARTESIAN_POINT('',(-1.2,-5.,7.));
#12980=CARTESIAN_POINT('Origin',(0.,-5.,7.));
#12981=CARTESIAN_POINT('Origin',(0.,-5.,7.));
#12982=CARTESIAN_POINT('',(-2.4,-4.8,7.));
#12983=CARTESIAN_POINT('Origin',(0.,-4.8,7.));
#12984=CARTESIAN_POINT('',(-2.4,-5.,7.));
#12985=CARTESIAN_POINT('',(-2.4,-5.,7.));
#12986=CARTESIAN_POINT('Origin',(0.,-5.,7.));
#12987=CARTESIAN_POINT('Origin',(0.,-4.8,7.));
#12988=CARTESIAN_POINT('Origin',(0.,-5.,7.));
#16951=UNCERTAINTY_MEASURE_WITH_UNIT(LENGTH_MEASURE(0.001),#17047,
'DISTANCE_ACCURACY_VALUE',
'Maximum model space distance between geometric entities at asserted c
onnectivities');
#16993=UNCERTAINTY_MEASURE_WITH_UNIT(LENGTH_MEASURE(0.001),#17047,
'DISTANCE_ACCURACY_VALUE',
'Maximum model space distance between geometric entities at asserted c
onnectivities');
#17004=(
GEOMETRIC_REPRESENTATION_CONTEXT(3)
GLOBAL_UNCERTAINTY_ASSIGNED_CONTEXT((#16951))
GLOBAL_UNIT_ASSIGNED_CONTEXT((#17047,#17049,#17050))
REPRESENTATION_CONTEXT('','3D')
);
#17046=(
GEOMETRIC_REPRESENTATION_CONTEXT(3)
GLOBAL_UNCERTAINTY_ASSIGNED_CONTEXT((#16993))
GLOBAL_UNIT_ASSIGNED_CONTEXT((#17047,#17049,#17050))
REPRESENTATION_CONTEXT('','3D')
);
#17047=(
LENGTH_UNIT()
NAMED_UNIT(*)
SI_UNIT(.CENTI.,.METRE.)
);
#17049=(
NAMED_UNIT(*)
PLANE_ANGLE_UNIT()
SI_UNIT($,.RADIAN.)
);
#17050=(
NAMED_UNIT(*)
SI_UNIT($,.STERADIAN.)
SOLID_ANGLE_UNIT()
);
#17061=SHAPE_DEFINITION_REPRESENTATION(#17113,#17268);
#17113=PRODUCT_DEFINITION_SHAPE('',$,#17321);
#17268=SHAPE_REPRESENTATION('',(#8960),#17004);
#17310=PRODUCT_DEFINITION_CONTEXT('part definition',#17468,'design');
#17321=PRODUCT_DEFINITION('Bearing cap (2)','Bearing cap (2)',#17373,#17310);
#17373=PRODUCT_DEFINITION_FORMATION('',$,#17480);
#17468=APPLICATION_CONTEXT(
'Core Data for Automotive Mechanical Design Process');
#17469=PRODUCT_CONTEXT('part definition',#17468,'mechanical');
#17480=PRODUCT('Bearing cap (2)','Bearing cap (2)','Bearing cap (2)',(#17469));
#17585=COLOUR_RGB('Grey',0.48,0.52,0.57);
#17586=FILL_AREA_STYLE_COLOUR('',#17585);
#17587=FILL_AREA_STYLE('',(#17586));
#17588=SURFACE_STYLE_FILL_AREA(#17587);
#17589=SURFACE_SIDE_STYLE('',(#17588));
#17590=SURFACE_STYLE_USAGE(.BOTH.,#17589);
#17591=PRESENTATION_STYLE_ASSIGNMENT((#17590));
ENDSEC;
END-ISO-10303-21;
